ISO-10303-21;
HEADER;
/* Generated by software containing ST-Developer
 * from STEP Tools, Inc. (www.steptools.com) 
 */

FILE_DESCRIPTION(
/* description */ (''),
/* implementation_level */ '2;1');

FILE_NAME(
/* name */ 'Wheel.step',
/* time_stamp */ '2026-09-20T21:58:27+06:00',
/* author */ (''),
/* organization */ (''),
/* preprocessor_version */ 'ST-DEVELOPER v20.2',
/* originating_system */ 'Autodesk Translation Framework v15.15.0.0',
/* authorisation */ '');

FILE_SCHEMA (('AUTOMOTIVE_DESIGN { 1 0 10303 214 3 1 1 }'));
ENDSEC;

DATA;
#10=MECHANICAL_DESIGN_GEOMETRIC_PRESENTATION_REPRESENTATION('',(#59),#2238);
#43=SHAPE_REPRESENTATION_RELATIONSHIP('SRR','None',#2270,#51);
#51=ADVANCED_BREP_SHAPE_REPRESENTATION('',(#67),#2230);
#59=STYLED_ITEM('',(#2319),#67);
#67=MANIFOLD_SOLID_BREP('Wheel',#1206);
#75=FACE_BOUND('',#201,.T.);
#76=FACE_BOUND('',#205,.T.);
#89=PLANE('',#1335);
#90=PLANE('',#1355);
#91=PLANE('',#1371);
#92=PLANE('',#1373);
#93=PLANE('',#1375);
#94=PLANE('',#1376);
#95=PLANE('',#1378);
#96=PLANE('',#1380);
#97=PLANE('',#1381);
#98=PLANE('',#1383);
#99=PLANE('',#1385);
#100=PLANE('',#1388);
#101=PLANE('',#1390);
#102=PLANE('',#1392);
#121=FACE_OUTER_BOUND('',#190,.T.);
#122=FACE_OUTER_BOUND('',#191,.T.);
#123=FACE_OUTER_BOUND('',#192,.T.);
#124=FACE_OUTER_BOUND('',#193,.T.);
#125=FACE_OUTER_BOUND('',#194,.T.);
#126=FACE_OUTER_BOUND('',#195,.T.);
#127=FACE_OUTER_BOUND('',#196,.T.);
#128=FACE_OUTER_BOUND('',#197,.T.);
#129=FACE_OUTER_BOUND('',#198,.T.);
#130=FACE_OUTER_BOUND('',#199,.T.);
#131=FACE_OUTER_BOUND('',#200,.T.);
#132=FACE_OUTER_BOUND('',#202,.T.);
#133=FACE_OUTER_BOUND('',#203,.T.);
#134=FACE_OUTER_BOUND('',#204,.T.);
#135=FACE_OUTER_BOUND('',#206,.T.);
#136=FACE_OUTER_BOUND('',#207,.T.);
#137=FACE_OUTER_BOUND('',#208,.T.);
#138=FACE_OUTER_BOUND('',#209,.T.);
#139=FACE_OUTER_BOUND('',#210,.T.);
#140=FACE_OUTER_BOUND('',#211,.T.);
#141=FACE_OUTER_BOUND('',#212,.T.);
#142=FACE_OUTER_BOUND('',#213,.T.);
#143=FACE_OUTER_BOUND('',#214,.T.);
#144=FACE_OUTER_BOUND('',#215,.T.);
#145=FACE_OUTER_BOUND('',#216,.T.);
#146=FACE_OUTER_BOUND('',#217,.T.);
#147=FACE_OUTER_BOUND('',#218,.T.);
#148=FACE_OUTER_BOUND('',#219,.T.);
#149=FACE_OUTER_BOUND('',#220,.T.);
#150=FACE_OUTER_BOUND('',#221,.T.);
#151=FACE_OUTER_BOUND('',#222,.T.);
#152=FACE_OUTER_BOUND('',#223,.T.);
#153=FACE_OUTER_BOUND('',#224,.T.);
#154=FACE_OUTER_BOUND('',#225,.T.);
#155=FACE_OUTER_BOUND('',#226,.T.);
#156=FACE_OUTER_BOUND('',#227,.T.);
#157=FACE_OUTER_BOUND('',#228,.T.);
#158=FACE_OUTER_BOUND('',#229,.T.);
#159=FACE_OUTER_BOUND('',#230,.T.);
#190=EDGE_LOOP('',(#782,#783,#784,#785));
#191=EDGE_LOOP('',(#786,#787,#788,#789));
#192=EDGE_LOOP('',(#790,#791,#792,#793));
#193=EDGE_LOOP('',(#794,#795,#796,#797));
#194=EDGE_LOOP('',(#798,#799,#800,#801));
#195=EDGE_LOOP('',(#802,#803,#804,#805));
#196=EDGE_LOOP('',(#806,#807,#808,#809));
#197=EDGE_LOOP('',(#810,#811,#812,#813));
#198=EDGE_LOOP('',(#814,#815,#816,#817));
#199=EDGE_LOOP('',(#818,#819,#820,#821));
#200=EDGE_LOOP('',(#822,#823,#824,#825,#826,#827,#828,#829,#830,#831,#832,
#833,#834,#835,#836,#837,#838,#839,#840,#841,#842,#843,#844,#845,#846,#847,
#848,#849,#850,#851,#852,#853,#854,#855,#856,#857));
#201=EDGE_LOOP('',(#858));
#202=EDGE_LOOP('',(#859,#860,#861,#862));
#203=EDGE_LOOP('',(#863,#864,#865,#866));
#204=EDGE_LOOP('',(#867,#868,#869,#870,#871,#872,#873,#874,#875,#876,#877,
#878,#879,#880,#881,#882,#883,#884,#885,#886,#887,#888,#889,#890,#891,#892,
#893,#894,#895,#896,#897,#898,#899,#900,#901,#902));
#205=EDGE_LOOP('',(#903));
#206=EDGE_LOOP('',(#904,#905,#906,#907));
#207=EDGE_LOOP('',(#908,#909,#910,#911));
#208=EDGE_LOOP('',(#912,#913,#914,#915));
#209=EDGE_LOOP('',(#916,#917,#918,#919));
#210=EDGE_LOOP('',(#920,#921,#922,#923));
#211=EDGE_LOOP('',(#924,#925,#926,#927));
#212=EDGE_LOOP('',(#928,#929,#930,#931));
#213=EDGE_LOOP('',(#932,#933,#934,#935));
#214=EDGE_LOOP('',(#936,#937,#938,#939));
#215=EDGE_LOOP('',(#940,#941,#942,#943));
#216=EDGE_LOOP('',(#944,#945,#946,#947));
#217=EDGE_LOOP('',(#948,#949,#950,#951));
#218=EDGE_LOOP('',(#952,#953,#954,#955));
#219=EDGE_LOOP('',(#956,#957,#958,#959));
#220=EDGE_LOOP('',(#960,#961,#962,#963));
#221=EDGE_LOOP('',(#964,#965,#966,#967));
#222=EDGE_LOOP('',(#968,#969,#970,#971));
#223=EDGE_LOOP('',(#972,#973,#974,#975));
#224=EDGE_LOOP('',(#976,#977,#978,#979));
#225=EDGE_LOOP('',(#980,#981,#982,#983));
#226=EDGE_LOOP('',(#984,#985,#986,#987));
#227=EDGE_LOOP('',(#988,#989,#990,#991));
#228=EDGE_LOOP('',(#992,#993,#994,#995));
#229=EDGE_LOOP('',(#996,#997,#998,#999));
#230=EDGE_LOOP('',(#1000,#1001,#1002,#1003));
#273=LINE('',#1874,#358);
#274=LINE('',#1879,#359);
#275=LINE('',#1883,#360);
#276=LINE('',#1888,#361);
#277=LINE('',#1892,#362);
#278=LINE('',#1897,#363);
#279=LINE('',#1901,#364);
#280=LINE('',#1906,#365);
#281=LINE('',#1910,#366);
#282=LINE('',#1915,#367);
#283=LINE('',#1919,#368);
#284=LINE('',#1925,#369);
#285=LINE('',#1931,#370);
#286=LINE('',#1937,#371);
#287=LINE('',#1943,#372);
#288=LINE('',#1947,#373);
#289=LINE('',#1951,#374);
#290=LINE('',#1954,#375);
#291=LINE('',#1958,#376);
#292=LINE('',#1961,#377);
#293=LINE('',#1965,#378);
#294=LINE('',#1968,#379);
#295=LINE('',#1972,#380);
#296=LINE('',#1977,#381);
#297=LINE('',#1981,#382);
#298=LINE('',#1989,#383);
#299=LINE('',#1993,#384);
#300=LINE('',#1998,#385);
#301=LINE('',#2001,#386);
#302=LINE('',#2003,#387);
#303=LINE('',#2009,#388);
#304=LINE('',#2013,#389);
#305=LINE('',#2018,#390);
#306=LINE('',#2021,#391);
#307=LINE('',#2025,#392);
#308=LINE('',#2028,#393);
#309=LINE('',#2032,#394);
#310=LINE('',#2035,#395);
#311=LINE('',#2039,#396);
#312=LINE('',#2042,#397);
#313=LINE('',#2046,#398);
#314=LINE('',#2049,#399);
#315=LINE('',#2051,#400);
#316=LINE('',#2053,#401);
#317=LINE('',#2055,#402);
#318=LINE('',#2057,#403);
#319=LINE('',#2059,#404);
#320=LINE('',#2062,#405);
#321=LINE('',#2064,#406);
#322=LINE('',#2066,#407);
#323=LINE('',#2069,#408);
#324=LINE('',#2071,#409);
#325=LINE('',#2073,#410);
#326=LINE('',#2074,#411);
#327=LINE('',#2076,#412);
#328=LINE('',#2079,#413);
#329=LINE('',#2081,#414);
#330=LINE('',#2085,#415);
#331=LINE('',#2087,#416);
#332=LINE('',#2089,#417);
#333=LINE('',#2092,#418);
#358=VECTOR('',#1471,2.5);
#359=VECTOR('',#1476,10.);
#360=VECTOR('',#1479,10.);
#361=VECTOR('',#1484,10.);
#362=VECTOR('',#1487,10.);
#363=VECTOR('',#1492,10.);
#364=VECTOR('',#1495,10.);
#365=VECTOR('',#1500,10.);
#366=VECTOR('',#1503,10.);
#367=VECTOR('',#1508,10.);
#368=VECTOR('',#1511,10.);
#369=VECTOR('',#1518,10.);
#370=VECTOR('',#1525,10.);
#371=VECTOR('',#1532,10.);
#372=VECTOR('',#1539,10.);
#373=VECTOR('',#1544,10.);
#374=VECTOR('',#1547,10.);
#375=VECTOR('',#1550,10.);
#376=VECTOR('',#1553,10.);
#377=VECTOR('',#1556,10.);
#378=VECTOR('',#1559,10.);
#379=VECTOR('',#1562,10.);
#380=VECTOR('',#1565,10.);
#381=VECTOR('',#1570,10.);
#382=VECTOR('',#1573,10.);
#383=VECTOR('',#1580,10.);
#384=VECTOR('',#1583,10.);
#385=VECTOR('',#1590,10.);
#386=VECTOR('',#1593,10.);
#387=VECTOR('',#1594,10.);
#388=VECTOR('',#1601,10.);
#389=VECTOR('',#1604,10.);
#390=VECTOR('',#1609,10.);
#391=VECTOR('',#1612,10.);
#392=VECTOR('',#1615,10.);
#393=VECTOR('',#1618,10.);
#394=VECTOR('',#1621,10.);
#395=VECTOR('',#1624,10.);
#396=VECTOR('',#1627,10.);
#397=VECTOR('',#1630,10.);
#398=VECTOR('',#1633,10.);
#399=VECTOR('',#1636,10.);
#400=VECTOR('',#1639,10.);
#401=VECTOR('',#1642,10.);
#402=VECTOR('',#1645,10.);
#403=VECTOR('',#1648,10.);
#404=VECTOR('',#1651,10.);
#405=VECTOR('',#1656,10.);
#406=VECTOR('',#1659,10.);
#407=VECTOR('',#1662,10.);
#408=VECTOR('',#1667,10.);
#409=VECTOR('',#1670,10.);
#410=VECTOR('',#1673,10.);
#411=VECTOR('',#1674,10.);
#412=VECTOR('',#1677,10.);
#413=VECTOR('',#1682,10.);
#414=VECTOR('',#1685,10.);
#415=VECTOR('',#1692,10.);
#416=VECTOR('',#1695,10.);
#417=VECTOR('',#1698,10.);
#418=VECTOR('',#1703,10.);
#443=CIRCLE('',#1306,2.5);
#444=CIRCLE('',#1307,2.5);
#445=CIRCLE('',#1309,13.);
#446=CIRCLE('',#1310,13.);
#447=CIRCLE('',#1312,13.);
#448=CIRCLE('',#1313,13.);
#449=CIRCLE('',#1315,13.);
#450=CIRCLE('',#1316,13.);
#451=CIRCLE('',#1318,13.);
#452=CIRCLE('',#1319,13.);
#453=CIRCLE('',#1321,13.);
#454=CIRCLE('',#1322,13.);
#455=CIRCLE('',#1324,35.);
#456=CIRCLE('',#1325,35.);
#457=CIRCLE('',#1327,35.);
#458=CIRCLE('',#1328,35.);
#459=CIRCLE('',#1330,35.);
#460=CIRCLE('',#1331,35.);
#461=CIRCLE('',#1333,35.);
#462=CIRCLE('',#1334,35.);
#463=CIRCLE('',#1336,2.5);
#464=CIRCLE('',#1337,35.);
#465=CIRCLE('',#1338,2.5);
#466=CIRCLE('',#1339,35.);
#467=CIRCLE('',#1340,2.5);
#468=CIRCLE('',#1341,35.);
#469=CIRCLE('',#1342,2.5);
#470=CIRCLE('',#1343,35.);
#471=CIRCLE('',#1344,35.);
#472=CIRCLE('',#1345,2.5);
#473=CIRCLE('',#1346,35.);
#474=CIRCLE('',#1347,13.);
#475=CIRCLE('',#1348,35.);
#476=CIRCLE('',#1349,2.5);
#477=CIRCLE('',#1350,35.);
#478=CIRCLE('',#1352,35.);
#479=CIRCLE('',#1354,13.);
#480=CIRCLE('',#1356,35.);
#481=CIRCLE('',#1357,2.5);
#482=CIRCLE('',#1358,35.);
#483=CIRCLE('',#1359,35.);
#484=CIRCLE('',#1360,2.5);
#485=CIRCLE('',#1361,35.);
#486=CIRCLE('',#1362,2.5);
#487=CIRCLE('',#1363,35.);
#488=CIRCLE('',#1364,2.5);
#489=CIRCLE('',#1365,35.);
#490=CIRCLE('',#1366,2.5);
#491=CIRCLE('',#1367,35.);
#492=CIRCLE('',#1368,2.5);
#517=VERTEX_POINT('',#1871);
#518=VERTEX_POINT('',#1873);
#519=VERTEX_POINT('',#1877);
#520=VERTEX_POINT('',#1878);
#521=VERTEX_POINT('',#1880);
#522=VERTEX_POINT('',#1882);
#523=VERTEX_POINT('',#1886);
#524=VERTEX_POINT('',#1887);
#525=VERTEX_POINT('',#1889);
#526=VERTEX_POINT('',#1891);
#527=VERTEX_POINT('',#1895);
#528=VERTEX_POINT('',#1896);
#529=VERTEX_POINT('',#1898);
#530=VERTEX_POINT('',#1900);
#531=VERTEX_POINT('',#1904);
#532=VERTEX_POINT('',#1905);
#533=VERTEX_POINT('',#1907);
#534=VERTEX_POINT('',#1909);
#535=VERTEX_POINT('',#1913);
#536=VERTEX_POINT('',#1914);
#537=VERTEX_POINT('',#1916);
#538=VERTEX_POINT('',#1918);
#539=VERTEX_POINT('',#1922);
#540=VERTEX_POINT('',#1924);
#541=VERTEX_POINT('',#1928);
#542=VERTEX_POINT('',#1930);
#543=VERTEX_POINT('',#1934);
#544=VERTEX_POINT('',#1936);
#545=VERTEX_POINT('',#1940);
#546=VERTEX_POINT('',#1942);
#547=VERTEX_POINT('',#1946);
#548=VERTEX_POINT('',#1948);
#549=VERTEX_POINT('',#1950);
#550=VERTEX_POINT('',#1953);
#551=VERTEX_POINT('',#1955);
#552=VERTEX_POINT('',#1957);
#553=VERTEX_POINT('',#1960);
#554=VERTEX_POINT('',#1962);
#555=VERTEX_POINT('',#1964);
#556=VERTEX_POINT('',#1967);
#557=VERTEX_POINT('',#1969);
#558=VERTEX_POINT('',#1971);
#559=VERTEX_POINT('',#1974);
#560=VERTEX_POINT('',#1976);
#561=VERTEX_POINT('',#1978);
#562=VERTEX_POINT('',#1980);
#563=VERTEX_POINT('',#1982);
#564=VERTEX_POINT('',#1984);
#565=VERTEX_POINT('',#1986);
#566=VERTEX_POINT('',#1988);
#567=VERTEX_POINT('',#1990);
#568=VERTEX_POINT('',#1992);
#569=VERTEX_POINT('',#1996);
#570=VERTEX_POINT('',#2000);
#571=VERTEX_POINT('',#2002);
#572=VERTEX_POINT('',#2006);
#573=VERTEX_POINT('',#2008);
#574=VERTEX_POINT('',#2010);
#575=VERTEX_POINT('',#2012);
#576=VERTEX_POINT('',#2015);
#577=VERTEX_POINT('',#2017);
#578=VERTEX_POINT('',#2019);
#579=VERTEX_POINT('',#2022);
#580=VERTEX_POINT('',#2024);
#581=VERTEX_POINT('',#2026);
#582=VERTEX_POINT('',#2029);
#583=VERTEX_POINT('',#2031);
#584=VERTEX_POINT('',#2033);
#585=VERTEX_POINT('',#2036);
#586=VERTEX_POINT('',#2038);
#587=VERTEX_POINT('',#2040);
#588=VERTEX_POINT('',#2043);
#589=VERTEX_POINT('',#2045);
#590=VERTEX_POINT('',#2047);
#623=EDGE_CURVE('',#517,#517,#443,.T.);
#624=EDGE_CURVE('',#517,#518,#273,.T.);
#625=EDGE_CURVE('',#518,#518,#444,.T.);
#626=EDGE_CURVE('',#519,#520,#274,.T.);
#627=EDGE_CURVE('',#521,#519,#445,.T.);
#628=EDGE_CURVE('',#522,#521,#275,.T.);
#629=EDGE_CURVE('',#520,#522,#446,.T.);
#630=EDGE_CURVE('',#523,#524,#276,.T.);
#631=EDGE_CURVE('',#525,#523,#447,.T.);
#632=EDGE_CURVE('',#526,#525,#277,.T.);
#633=EDGE_CURVE('',#524,#526,#448,.T.);
#634=EDGE_CURVE('',#527,#528,#278,.T.);
#635=EDGE_CURVE('',#529,#527,#449,.T.);
#636=EDGE_CURVE('',#530,#529,#279,.T.);
#637=EDGE_CURVE('',#528,#530,#450,.T.);
#638=EDGE_CURVE('',#531,#532,#280,.T.);
#639=EDGE_CURVE('',#533,#531,#451,.T.);
#640=EDGE_CURVE('',#534,#533,#281,.T.);
#641=EDGE_CURVE('',#532,#534,#452,.T.);
#642=EDGE_CURVE('',#535,#536,#282,.T.);
#643=EDGE_CURVE('',#537,#535,#453,.T.);
#644=EDGE_CURVE('',#538,#537,#283,.T.);
#645=EDGE_CURVE('',#536,#538,#454,.T.);
#646=EDGE_CURVE('',#539,#521,#455,.T.);
#647=EDGE_CURVE('',#540,#539,#284,.T.);
#648=EDGE_CURVE('',#522,#540,#456,.T.);
#649=EDGE_CURVE('',#525,#541,#457,.T.);
#650=EDGE_CURVE('',#542,#541,#285,.T.);
#651=EDGE_CURVE('',#542,#526,#458,.T.);
#652=EDGE_CURVE('',#543,#529,#459,.T.);
#653=EDGE_CURVE('',#544,#543,#286,.T.);
#654=EDGE_CURVE('',#530,#544,#460,.T.);
#655=EDGE_CURVE('',#545,#533,#461,.T.);
#656=EDGE_CURVE('',#546,#545,#287,.T.);
#657=EDGE_CURVE('',#534,#546,#462,.T.);
#658=EDGE_CURVE('',#547,#540,#288,.T.);
#659=EDGE_CURVE('',#547,#548,#463,.T.);
#660=EDGE_CURVE('',#548,#549,#289,.T.);
#661=EDGE_CURVE('',#524,#549,#464,.T.);
#662=EDGE_CURVE('',#542,#550,#290,.T.);
#663=EDGE_CURVE('',#550,#551,#465,.T.);
#664=EDGE_CURVE('',#551,#552,#291,.T.);
#665=EDGE_CURVE('',#552,#528,#466,.T.);
#666=EDGE_CURVE('',#553,#544,#292,.T.);
#667=EDGE_CURVE('',#554,#553,#467,.T.);
#668=EDGE_CURVE('',#555,#554,#293,.T.);
#669=EDGE_CURVE('',#555,#532,#468,.T.);
#670=EDGE_CURVE('',#556,#546,#294,.T.);
#671=EDGE_CURVE('',#557,#556,#469,.T.);
#672=EDGE_CURVE('',#557,#558,#295,.T.);
#673=EDGE_CURVE('',#536,#558,#470,.T.);
#674=EDGE_CURVE('',#559,#538,#471,.T.);
#675=EDGE_CURVE('',#559,#560,#296,.T.);
#676=EDGE_CURVE('',#560,#561,#472,.T.);
#677=EDGE_CURVE('',#561,#562,#297,.T.);
#678=EDGE_CURVE('',#563,#562,#473,.T.);
#679=EDGE_CURVE('',#563,#564,#474,.T.);
#680=EDGE_CURVE('',#565,#564,#475,.T.);
#681=EDGE_CURVE('',#566,#565,#298,.T.);
#682=EDGE_CURVE('',#567,#566,#476,.T.);
#683=EDGE_CURVE('',#568,#567,#299,.T.);
#684=EDGE_CURVE('',#568,#520,#477,.T.);
#685=EDGE_CURVE('',#537,#569,#478,.T.);
#686=EDGE_CURVE('',#559,#569,#300,.T.);
#687=EDGE_CURVE('',#564,#570,#301,.T.);
#688=EDGE_CURVE('',#571,#563,#302,.T.);
#689=EDGE_CURVE('',#570,#571,#479,.T.);
#690=EDGE_CURVE('',#519,#572,#480,.T.);
#691=EDGE_CURVE('',#572,#573,#303,.T.);
#692=EDGE_CURVE('',#573,#574,#481,.T.);
#693=EDGE_CURVE('',#574,#575,#304,.T.);
#694=EDGE_CURVE('',#570,#575,#482,.T.);
#695=EDGE_CURVE('',#576,#571,#483,.T.);
#696=EDGE_CURVE('',#577,#576,#305,.T.);
#697=EDGE_CURVE('',#578,#577,#484,.T.);
#698=EDGE_CURVE('',#569,#578,#306,.T.);
#699=EDGE_CURVE('',#579,#535,#485,.T.);
#700=EDGE_CURVE('',#580,#579,#307,.T.);
#701=EDGE_CURVE('',#581,#580,#486,.T.);
#702=EDGE_CURVE('',#581,#545,#308,.T.);
#703=EDGE_CURVE('',#531,#582,#487,.T.);
#704=EDGE_CURVE('',#582,#583,#309,.T.);
#705=EDGE_CURVE('',#583,#584,#488,.T.);
#706=EDGE_CURVE('',#584,#543,#310,.T.);
#707=EDGE_CURVE('',#527,#585,#489,.T.);
#708=EDGE_CURVE('',#586,#585,#311,.T.);
#709=EDGE_CURVE('',#587,#586,#490,.T.);
#710=EDGE_CURVE('',#541,#587,#312,.T.);
#711=EDGE_CURVE('',#588,#523,#491,.T.);
#712=EDGE_CURVE('',#589,#588,#313,.T.);
#713=EDGE_CURVE('',#589,#590,#492,.T.);
#714=EDGE_CURVE('',#590,#539,#314,.T.);
#715=EDGE_CURVE('',#562,#576,#315,.T.);
#716=EDGE_CURVE('',#565,#575,#316,.T.);
#717=EDGE_CURVE('',#566,#574,#317,.T.);
#718=EDGE_CURVE('',#567,#573,#318,.T.);
#719=EDGE_CURVE('',#568,#572,#319,.T.);
#720=EDGE_CURVE('',#547,#590,#320,.T.);
#721=EDGE_CURVE('',#561,#577,#321,.T.);
#722=EDGE_CURVE('',#560,#578,#322,.T.);
#723=EDGE_CURVE('',#558,#579,#323,.T.);
#724=EDGE_CURVE('',#557,#580,#324,.T.);
#725=EDGE_CURVE('',#551,#586,#325,.T.);
#726=EDGE_CURVE('',#552,#585,#326,.T.);
#727=EDGE_CURVE('',#550,#587,#327,.T.);
#728=EDGE_CURVE('',#549,#588,#328,.T.);
#729=EDGE_CURVE('',#548,#589,#329,.T.);
#730=EDGE_CURVE('',#553,#584,#330,.T.);
#731=EDGE_CURVE('',#554,#583,#331,.T.);
#732=EDGE_CURVE('',#555,#582,#332,.T.);
#733=EDGE_CURVE('',#556,#581,#333,.T.);
#782=ORIENTED_EDGE('',*,*,#623,.F.);
#783=ORIENTED_EDGE('',*,*,#624,.T.);
#784=ORIENTED_EDGE('',*,*,#625,.F.);
#785=ORIENTED_EDGE('',*,*,#624,.F.);
#786=ORIENTED_EDGE('',*,*,#626,.F.);
#787=ORIENTED_EDGE('',*,*,#627,.F.);
#788=ORIENTED_EDGE('',*,*,#628,.F.);
#789=ORIENTED_EDGE('',*,*,#629,.F.);
#790=ORIENTED_EDGE('',*,*,#630,.F.);
#791=ORIENTED_EDGE('',*,*,#631,.F.);
#792=ORIENTED_EDGE('',*,*,#632,.F.);
#793=ORIENTED_EDGE('',*,*,#633,.F.);
#794=ORIENTED_EDGE('',*,*,#634,.F.);
#795=ORIENTED_EDGE('',*,*,#635,.F.);
#796=ORIENTED_EDGE('',*,*,#636,.F.);
#797=ORIENTED_EDGE('',*,*,#637,.F.);
#798=ORIENTED_EDGE('',*,*,#638,.F.);
#799=ORIENTED_EDGE('',*,*,#639,.F.);
#800=ORIENTED_EDGE('',*,*,#640,.F.);
#801=ORIENTED_EDGE('',*,*,#641,.F.);
#802=ORIENTED_EDGE('',*,*,#642,.F.);
#803=ORIENTED_EDGE('',*,*,#643,.F.);
#804=ORIENTED_EDGE('',*,*,#644,.F.);
#805=ORIENTED_EDGE('',*,*,#645,.F.);
#806=ORIENTED_EDGE('',*,*,#628,.T.);
#807=ORIENTED_EDGE('',*,*,#646,.F.);
#808=ORIENTED_EDGE('',*,*,#647,.F.);
#809=ORIENTED_EDGE('',*,*,#648,.F.);
#810=ORIENTED_EDGE('',*,*,#632,.T.);
#811=ORIENTED_EDGE('',*,*,#649,.T.);
#812=ORIENTED_EDGE('',*,*,#650,.F.);
#813=ORIENTED_EDGE('',*,*,#651,.T.);
#814=ORIENTED_EDGE('',*,*,#636,.T.);
#815=ORIENTED_EDGE('',*,*,#652,.F.);
#816=ORIENTED_EDGE('',*,*,#653,.F.);
#817=ORIENTED_EDGE('',*,*,#654,.F.);
#818=ORIENTED_EDGE('',*,*,#640,.T.);
#819=ORIENTED_EDGE('',*,*,#655,.F.);
#820=ORIENTED_EDGE('',*,*,#656,.F.);
#821=ORIENTED_EDGE('',*,*,#657,.F.);
#822=ORIENTED_EDGE('',*,*,#629,.T.);
#823=ORIENTED_EDGE('',*,*,#648,.T.);
#824=ORIENTED_EDGE('',*,*,#658,.F.);
#825=ORIENTED_EDGE('',*,*,#659,.T.);
#826=ORIENTED_EDGE('',*,*,#660,.T.);
#827=ORIENTED_EDGE('',*,*,#661,.F.);
#828=ORIENTED_EDGE('',*,*,#633,.T.);
#829=ORIENTED_EDGE('',*,*,#651,.F.);
#830=ORIENTED_EDGE('',*,*,#662,.T.);
#831=ORIENTED_EDGE('',*,*,#663,.T.);
#832=ORIENTED_EDGE('',*,*,#664,.T.);
#833=ORIENTED_EDGE('',*,*,#665,.T.);
#834=ORIENTED_EDGE('',*,*,#637,.T.);
#835=ORIENTED_EDGE('',*,*,#654,.T.);
#836=ORIENTED_EDGE('',*,*,#666,.F.);
#837=ORIENTED_EDGE('',*,*,#667,.F.);
#838=ORIENTED_EDGE('',*,*,#668,.F.);
#839=ORIENTED_EDGE('',*,*,#669,.T.);
#840=ORIENTED_EDGE('',*,*,#641,.T.);
#841=ORIENTED_EDGE('',*,*,#657,.T.);
#842=ORIENTED_EDGE('',*,*,#670,.F.);
#843=ORIENTED_EDGE('',*,*,#671,.F.);
#844=ORIENTED_EDGE('',*,*,#672,.T.);
#845=ORIENTED_EDGE('',*,*,#673,.F.);
#846=ORIENTED_EDGE('',*,*,#645,.T.);
#847=ORIENTED_EDGE('',*,*,#674,.F.);
#848=ORIENTED_EDGE('',*,*,#675,.T.);
#849=ORIENTED_EDGE('',*,*,#676,.T.);
#850=ORIENTED_EDGE('',*,*,#677,.T.);
#851=ORIENTED_EDGE('',*,*,#678,.F.);
#852=ORIENTED_EDGE('',*,*,#679,.T.);
#853=ORIENTED_EDGE('',*,*,#680,.F.);
#854=ORIENTED_EDGE('',*,*,#681,.F.);
#855=ORIENTED_EDGE('',*,*,#682,.F.);
#856=ORIENTED_EDGE('',*,*,#683,.F.);
#857=ORIENTED_EDGE('',*,*,#684,.T.);
#858=ORIENTED_EDGE('',*,*,#623,.T.);
#859=ORIENTED_EDGE('',*,*,#644,.T.);
#860=ORIENTED_EDGE('',*,*,#685,.T.);
#861=ORIENTED_EDGE('',*,*,#686,.F.);
#862=ORIENTED_EDGE('',*,*,#674,.T.);
#863=ORIENTED_EDGE('',*,*,#687,.F.);
#864=ORIENTED_EDGE('',*,*,#679,.F.);
#865=ORIENTED_EDGE('',*,*,#688,.F.);
#866=ORIENTED_EDGE('',*,*,#689,.F.);
#867=ORIENTED_EDGE('',*,*,#627,.T.);
#868=ORIENTED_EDGE('',*,*,#690,.T.);
#869=ORIENTED_EDGE('',*,*,#691,.T.);
#870=ORIENTED_EDGE('',*,*,#692,.T.);
#871=ORIENTED_EDGE('',*,*,#693,.T.);
#872=ORIENTED_EDGE('',*,*,#694,.F.);
#873=ORIENTED_EDGE('',*,*,#689,.T.);
#874=ORIENTED_EDGE('',*,*,#695,.F.);
#875=ORIENTED_EDGE('',*,*,#696,.F.);
#876=ORIENTED_EDGE('',*,*,#697,.F.);
#877=ORIENTED_EDGE('',*,*,#698,.F.);
#878=ORIENTED_EDGE('',*,*,#685,.F.);
#879=ORIENTED_EDGE('',*,*,#643,.T.);
#880=ORIENTED_EDGE('',*,*,#699,.F.);
#881=ORIENTED_EDGE('',*,*,#700,.F.);
#882=ORIENTED_EDGE('',*,*,#701,.F.);
#883=ORIENTED_EDGE('',*,*,#702,.T.);
#884=ORIENTED_EDGE('',*,*,#655,.T.);
#885=ORIENTED_EDGE('',*,*,#639,.T.);
#886=ORIENTED_EDGE('',*,*,#703,.T.);
#887=ORIENTED_EDGE('',*,*,#704,.T.);
#888=ORIENTED_EDGE('',*,*,#705,.T.);
#889=ORIENTED_EDGE('',*,*,#706,.T.);
#890=ORIENTED_EDGE('',*,*,#652,.T.);
#891=ORIENTED_EDGE('',*,*,#635,.T.);
#892=ORIENTED_EDGE('',*,*,#707,.T.);
#893=ORIENTED_EDGE('',*,*,#708,.F.);
#894=ORIENTED_EDGE('',*,*,#709,.F.);
#895=ORIENTED_EDGE('',*,*,#710,.F.);
#896=ORIENTED_EDGE('',*,*,#649,.F.);
#897=ORIENTED_EDGE('',*,*,#631,.T.);
#898=ORIENTED_EDGE('',*,*,#711,.F.);
#899=ORIENTED_EDGE('',*,*,#712,.F.);
#900=ORIENTED_EDGE('',*,*,#713,.T.);
#901=ORIENTED_EDGE('',*,*,#714,.T.);
#902=ORIENTED_EDGE('',*,*,#646,.T.);
#903=ORIENTED_EDGE('',*,*,#625,.T.);
#904=ORIENTED_EDGE('',*,*,#688,.T.);
#905=ORIENTED_EDGE('',*,*,#678,.T.);
#906=ORIENTED_EDGE('',*,*,#715,.T.);
#907=ORIENTED_EDGE('',*,*,#695,.T.);
#908=ORIENTED_EDGE('',*,*,#687,.T.);
#909=ORIENTED_EDGE('',*,*,#694,.T.);
#910=ORIENTED_EDGE('',*,*,#716,.F.);
#911=ORIENTED_EDGE('',*,*,#680,.T.);
#912=ORIENTED_EDGE('',*,*,#681,.T.);
#913=ORIENTED_EDGE('',*,*,#716,.T.);
#914=ORIENTED_EDGE('',*,*,#693,.F.);
#915=ORIENTED_EDGE('',*,*,#717,.F.);
#916=ORIENTED_EDGE('',*,*,#682,.T.);
#917=ORIENTED_EDGE('',*,*,#717,.T.);
#918=ORIENTED_EDGE('',*,*,#692,.F.);
#919=ORIENTED_EDGE('',*,*,#718,.F.);
#920=ORIENTED_EDGE('',*,*,#683,.T.);
#921=ORIENTED_EDGE('',*,*,#718,.T.);
#922=ORIENTED_EDGE('',*,*,#691,.F.);
#923=ORIENTED_EDGE('',*,*,#719,.F.);
#924=ORIENTED_EDGE('',*,*,#626,.T.);
#925=ORIENTED_EDGE('',*,*,#684,.F.);
#926=ORIENTED_EDGE('',*,*,#719,.T.);
#927=ORIENTED_EDGE('',*,*,#690,.F.);
#928=ORIENTED_EDGE('',*,*,#658,.T.);
#929=ORIENTED_EDGE('',*,*,#647,.T.);
#930=ORIENTED_EDGE('',*,*,#714,.F.);
#931=ORIENTED_EDGE('',*,*,#720,.F.);
#932=ORIENTED_EDGE('',*,*,#677,.F.);
#933=ORIENTED_EDGE('',*,*,#721,.T.);
#934=ORIENTED_EDGE('',*,*,#696,.T.);
#935=ORIENTED_EDGE('',*,*,#715,.F.);
#936=ORIENTED_EDGE('',*,*,#676,.F.);
#937=ORIENTED_EDGE('',*,*,#722,.T.);
#938=ORIENTED_EDGE('',*,*,#697,.T.);
#939=ORIENTED_EDGE('',*,*,#721,.F.);
#940=ORIENTED_EDGE('',*,*,#675,.F.);
#941=ORIENTED_EDGE('',*,*,#686,.T.);
#942=ORIENTED_EDGE('',*,*,#698,.T.);
#943=ORIENTED_EDGE('',*,*,#722,.F.);
#944=ORIENTED_EDGE('',*,*,#642,.T.);
#945=ORIENTED_EDGE('',*,*,#673,.T.);
#946=ORIENTED_EDGE('',*,*,#723,.T.);
#947=ORIENTED_EDGE('',*,*,#699,.T.);
#948=ORIENTED_EDGE('',*,*,#672,.F.);
#949=ORIENTED_EDGE('',*,*,#724,.T.);
#950=ORIENTED_EDGE('',*,*,#700,.T.);
#951=ORIENTED_EDGE('',*,*,#723,.F.);
#952=ORIENTED_EDGE('',*,*,#664,.F.);
#953=ORIENTED_EDGE('',*,*,#725,.T.);
#954=ORIENTED_EDGE('',*,*,#708,.T.);
#955=ORIENTED_EDGE('',*,*,#726,.F.);
#956=ORIENTED_EDGE('',*,*,#663,.F.);
#957=ORIENTED_EDGE('',*,*,#727,.T.);
#958=ORIENTED_EDGE('',*,*,#709,.T.);
#959=ORIENTED_EDGE('',*,*,#725,.F.);
#960=ORIENTED_EDGE('',*,*,#662,.F.);
#961=ORIENTED_EDGE('',*,*,#650,.T.);
#962=ORIENTED_EDGE('',*,*,#710,.T.);
#963=ORIENTED_EDGE('',*,*,#727,.F.);
#964=ORIENTED_EDGE('',*,*,#630,.T.);
#965=ORIENTED_EDGE('',*,*,#661,.T.);
#966=ORIENTED_EDGE('',*,*,#728,.T.);
#967=ORIENTED_EDGE('',*,*,#711,.T.);
#968=ORIENTED_EDGE('',*,*,#660,.F.);
#969=ORIENTED_EDGE('',*,*,#729,.T.);
#970=ORIENTED_EDGE('',*,*,#712,.T.);
#971=ORIENTED_EDGE('',*,*,#728,.F.);
#972=ORIENTED_EDGE('',*,*,#659,.F.);
#973=ORIENTED_EDGE('',*,*,#720,.T.);
#974=ORIENTED_EDGE('',*,*,#713,.F.);
#975=ORIENTED_EDGE('',*,*,#729,.F.);
#976=ORIENTED_EDGE('',*,*,#634,.T.);
#977=ORIENTED_EDGE('',*,*,#665,.F.);
#978=ORIENTED_EDGE('',*,*,#726,.T.);
#979=ORIENTED_EDGE('',*,*,#707,.F.);
#980=ORIENTED_EDGE('',*,*,#666,.T.);
#981=ORIENTED_EDGE('',*,*,#653,.T.);
#982=ORIENTED_EDGE('',*,*,#706,.F.);
#983=ORIENTED_EDGE('',*,*,#730,.F.);
#984=ORIENTED_EDGE('',*,*,#667,.T.);
#985=ORIENTED_EDGE('',*,*,#730,.T.);
#986=ORIENTED_EDGE('',*,*,#705,.F.);
#987=ORIENTED_EDGE('',*,*,#731,.F.);
#988=ORIENTED_EDGE('',*,*,#668,.T.);
#989=ORIENTED_EDGE('',*,*,#731,.T.);
#990=ORIENTED_EDGE('',*,*,#704,.F.);
#991=ORIENTED_EDGE('',*,*,#732,.F.);
#992=ORIENTED_EDGE('',*,*,#638,.T.);
#993=ORIENTED_EDGE('',*,*,#669,.F.);
#994=ORIENTED_EDGE('',*,*,#732,.T.);
#995=ORIENTED_EDGE('',*,*,#703,.F.);
#996=ORIENTED_EDGE('',*,*,#670,.T.);
#997=ORIENTED_EDGE('',*,*,#656,.T.);
#998=ORIENTED_EDGE('',*,*,#702,.F.);
#999=ORIENTED_EDGE('',*,*,#733,.F.);
#1000=ORIENTED_EDGE('',*,*,#671,.T.);
#1001=ORIENTED_EDGE('',*,*,#733,.T.);
#1002=ORIENTED_EDGE('',*,*,#701,.T.);
#1003=ORIENTED_EDGE('',*,*,#724,.F.);
#1100=CYLINDRICAL_SURFACE('',#1305,2.5);
#1101=CYLINDRICAL_SURFACE('',#1308,13.);
#1102=CYLINDRICAL_SURFACE('',#1311,13.);
#1103=CYLINDRICAL_SURFACE('',#1314,13.);
#1104=CYLINDRICAL_SURFACE('',#1317,13.);
#1105=CYLINDRICAL_SURFACE('',#1320,13.);
#1106=CYLINDRICAL_SURFACE('',#1323,35.);
#1107=CYLINDRICAL_SURFACE('',#1326,35.);
#1108=CYLINDRICAL_SURFACE('',#1329,35.);
#1109=CYLINDRICAL_SURFACE('',#1332,35.);
#1110=CYLINDRICAL_SURFACE('',#1351,35.);
#1111=CYLINDRICAL_SURFACE('',#1353,13.);
#1112=CYLINDRICAL_SURFACE('',#1369,35.);
#1113=CYLINDRICAL_SURFACE('',#1370,35.);
#1114=CYLINDRICAL_SURFACE('',#1372,2.5);
#1115=CYLINDRICAL_SURFACE('',#1374,35.);
#1116=CYLINDRICAL_SURFACE('',#1377,2.5);
#1117=CYLINDRICAL_SURFACE('',#1379,35.);
#1118=CYLINDRICAL_SURFACE('',#1382,2.5);
#1119=CYLINDRICAL_SURFACE('',#1384,35.);
#1120=CYLINDRICAL_SURFACE('',#1386,2.5);
#1121=CYLINDRICAL_SURFACE('',#1387,35.);
#1122=CYLINDRICAL_SURFACE('',#1389,2.5);
#1123=CYLINDRICAL_SURFACE('',#1391,35.);
#1124=CYLINDRICAL_SURFACE('',#1393,2.5);
#1137=ADVANCED_FACE('',(#121),#1100,.F.);
#1138=ADVANCED_FACE('',(#122),#1101,.F.);
#1139=ADVANCED_FACE('',(#123),#1102,.F.);
#1140=ADVANCED_FACE('',(#124),#1103,.F.);
#1141=ADVANCED_FACE('',(#125),#1104,.F.);
#1142=ADVANCED_FACE('',(#126),#1105,.F.);
#1143=ADVANCED_FACE('',(#127),#1106,.T.);
#1144=ADVANCED_FACE('',(#128),#1107,.T.);
#1145=ADVANCED_FACE('',(#129),#1108,.T.);
#1146=ADVANCED_FACE('',(#130),#1109,.T.);
#1147=ADVANCED_FACE('',(#131,#75),#89,.T.);
#1148=ADVANCED_FACE('',(#132),#1110,.T.);
#1149=ADVANCED_FACE('',(#133),#1111,.F.);
#1150=ADVANCED_FACE('',(#134,#76),#90,.F.);
#1151=ADVANCED_FACE('',(#135),#1112,.T.);
#1152=ADVANCED_FACE('',(#136),#1113,.T.);
#1153=ADVANCED_FACE('',(#137),#91,.T.);
#1154=ADVANCED_FACE('',(#138),#1114,.F.);
#1155=ADVANCED_FACE('',(#139),#92,.T.);
#1156=ADVANCED_FACE('',(#140),#1115,.T.);
#1157=ADVANCED_FACE('',(#141),#93,.T.);
#1158=ADVANCED_FACE('',(#142),#94,.F.);
#1159=ADVANCED_FACE('',(#143),#1116,.F.);
#1160=ADVANCED_FACE('',(#144),#95,.F.);
#1161=ADVANCED_FACE('',(#145),#1117,.T.);
#1162=ADVANCED_FACE('',(#146),#96,.F.);
#1163=ADVANCED_FACE('',(#147),#97,.F.);
#1164=ADVANCED_FACE('',(#148),#1118,.F.);
#1165=ADVANCED_FACE('',(#149),#98,.F.);
#1166=ADVANCED_FACE('',(#150),#1119,.T.);
#1167=ADVANCED_FACE('',(#151),#99,.F.);
#1168=ADVANCED_FACE('',(#152),#1120,.F.);
#1169=ADVANCED_FACE('',(#153),#1121,.T.);
#1170=ADVANCED_FACE('',(#154),#100,.T.);
#1171=ADVANCED_FACE('',(#155),#1122,.F.);
#1172=ADVANCED_FACE('',(#156),#101,.T.);
#1173=ADVANCED_FACE('',(#157),#1123,.T.);
#1174=ADVANCED_FACE('',(#158),#102,.T.);
#1175=ADVANCED_FACE('',(#159),#1124,.F.);
#1206=CLOSED_SHELL('',(#1137,#1138,#1139,#1140,#1141,#1142,#1143,#1144,
#1145,#1146,#1147,#1148,#1149,#1150,#1151,#1152,#1153,#1154,#1155,#1156,
#1157,#1158,#1159,#1160,#1161,#1162,#1163,#1164,#1165,#1166,#1167,#1168,
#1169,#1170,#1171,#1172,#1173,#1174,#1175));
#1304=AXIS2_PLACEMENT_3D('',#1869,#1465,#1466);
#1305=AXIS2_PLACEMENT_3D('',#1870,#1467,#1468);
#1306=AXIS2_PLACEMENT_3D('',#1872,#1469,#1470);
#1307=AXIS2_PLACEMENT_3D('',#1875,#1472,#1473);
#1308=AXIS2_PLACEMENT_3D('',#1876,#1474,#1475);
#1309=AXIS2_PLACEMENT_3D('',#1881,#1477,#1478);
#1310=AXIS2_PLACEMENT_3D('',#1884,#1480,#1481);
#1311=AXIS2_PLACEMENT_3D('',#1885,#1482,#1483);
#1312=AXIS2_PLACEMENT_3D('',#1890,#1485,#1486);
#1313=AXIS2_PLACEMENT_3D('',#1893,#1488,#1489);
#1314=AXIS2_PLACEMENT_3D('',#1894,#1490,#1491);
#1315=AXIS2_PLACEMENT_3D('',#1899,#1493,#1494);
#1316=AXIS2_PLACEMENT_3D('',#1902,#1496,#1497);
#1317=AXIS2_PLACEMENT_3D('',#1903,#1498,#1499);
#1318=AXIS2_PLACEMENT_3D('',#1908,#1501,#1502);
#1319=AXIS2_PLACEMENT_3D('',#1911,#1504,#1505);
#1320=AXIS2_PLACEMENT_3D('',#1912,#1506,#1507);
#1321=AXIS2_PLACEMENT_3D('',#1917,#1509,#1510);
#1322=AXIS2_PLACEMENT_3D('',#1920,#1512,#1513);
#1323=AXIS2_PLACEMENT_3D('',#1921,#1514,#1515);
#1324=AXIS2_PLACEMENT_3D('',#1923,#1516,#1517);
#1325=AXIS2_PLACEMENT_3D('',#1926,#1519,#1520);
#1326=AXIS2_PLACEMENT_3D('',#1927,#1521,#1522);
#1327=AXIS2_PLACEMENT_3D('',#1929,#1523,#1524);
#1328=AXIS2_PLACEMENT_3D('',#1932,#1526,#1527);
#1329=AXIS2_PLACEMENT_3D('',#1933,#1528,#1529);
#1330=AXIS2_PLACEMENT_3D('',#1935,#1530,#1531);
#1331=AXIS2_PLACEMENT_3D('',#1938,#1533,#1534);
#1332=AXIS2_PLACEMENT_3D('',#1939,#1535,#1536);
#1333=AXIS2_PLACEMENT_3D('',#1941,#1537,#1538);
#1334=AXIS2_PLACEMENT_3D('',#1944,#1540,#1541);
#1335=AXIS2_PLACEMENT_3D('',#1945,#1542,#1543);
#1336=AXIS2_PLACEMENT_3D('',#1949,#1545,#1546);
#1337=AXIS2_PLACEMENT_3D('',#1952,#1548,#1549);
#1338=AXIS2_PLACEMENT_3D('',#1956,#1551,#1552);
#1339=AXIS2_PLACEMENT_3D('',#1959,#1554,#1555);
#1340=AXIS2_PLACEMENT_3D('',#1963,#1557,#1558);
#1341=AXIS2_PLACEMENT_3D('',#1966,#1560,#1561);
#1342=AXIS2_PLACEMENT_3D('',#1970,#1563,#1564);
#1343=AXIS2_PLACEMENT_3D('',#1973,#1566,#1567);
#1344=AXIS2_PLACEMENT_3D('',#1975,#1568,#1569);
#1345=AXIS2_PLACEMENT_3D('',#1979,#1571,#1572);
#1346=AXIS2_PLACEMENT_3D('',#1983,#1574,#1575);
#1347=AXIS2_PLACEMENT_3D('',#1985,#1576,#1577);
#1348=AXIS2_PLACEMENT_3D('',#1987,#1578,#1579);
#1349=AXIS2_PLACEMENT_3D('',#1991,#1581,#1582);
#1350=AXIS2_PLACEMENT_3D('',#1994,#1584,#1585);
#1351=AXIS2_PLACEMENT_3D('',#1995,#1586,#1587);
#1352=AXIS2_PLACEMENT_3D('',#1997,#1588,#1589);
#1353=AXIS2_PLACEMENT_3D('',#1999,#1591,#1592);
#1354=AXIS2_PLACEMENT_3D('',#2004,#1595,#1596);
#1355=AXIS2_PLACEMENT_3D('',#2005,#1597,#1598);
#1356=AXIS2_PLACEMENT_3D('',#2007,#1599,#1600);
#1357=AXIS2_PLACEMENT_3D('',#2011,#1602,#1603);
#1358=AXIS2_PLACEMENT_3D('',#2014,#1605,#1606);
#1359=AXIS2_PLACEMENT_3D('',#2016,#1607,#1608);
#1360=AXIS2_PLACEMENT_3D('',#2020,#1610,#1611);
#1361=AXIS2_PLACEMENT_3D('',#2023,#1613,#1614);
#1362=AXIS2_PLACEMENT_3D('',#2027,#1616,#1617);
#1363=AXIS2_PLACEMENT_3D('',#2030,#1619,#1620);
#1364=AXIS2_PLACEMENT_3D('',#2034,#1622,#1623);
#1365=AXIS2_PLACEMENT_3D('',#2037,#1625,#1626);
#1366=AXIS2_PLACEMENT_3D('',#2041,#1628,#1629);
#1367=AXIS2_PLACEMENT_3D('',#2044,#1631,#1632);
#1368=AXIS2_PLACEMENT_3D('',#2048,#1634,#1635);
#1369=AXIS2_PLACEMENT_3D('',#2050,#1637,#1638);
#1370=AXIS2_PLACEMENT_3D('',#2052,#1640,#1641);
#1371=AXIS2_PLACEMENT_3D('',#2054,#1643,#1644);
#1372=AXIS2_PLACEMENT_3D('',#2056,#1646,#1647);
#1373=AXIS2_PLACEMENT_3D('',#2058,#1649,#1650);
#1374=AXIS2_PLACEMENT_3D('',#2060,#1652,#1653);
#1375=AXIS2_PLACEMENT_3D('',#2061,#1654,#1655);
#1376=AXIS2_PLACEMENT_3D('',#2063,#1657,#1658);
#1377=AXIS2_PLACEMENT_3D('',#2065,#1660,#1661);
#1378=AXIS2_PLACEMENT_3D('',#2067,#1663,#1664);
#1379=AXIS2_PLACEMENT_3D('',#2068,#1665,#1666);
#1380=AXIS2_PLACEMENT_3D('',#2070,#1668,#1669);
#1381=AXIS2_PLACEMENT_3D('',#2072,#1671,#1672);
#1382=AXIS2_PLACEMENT_3D('',#2075,#1675,#1676);
#1383=AXIS2_PLACEMENT_3D('',#2077,#1678,#1679);
#1384=AXIS2_PLACEMENT_3D('',#2078,#1680,#1681);
#1385=AXIS2_PLACEMENT_3D('',#2080,#1683,#1684);
#1386=AXIS2_PLACEMENT_3D('',#2082,#1686,#1687);
#1387=AXIS2_PLACEMENT_3D('',#2083,#1688,#1689);
#1388=AXIS2_PLACEMENT_3D('',#2084,#1690,#1691);
#1389=AXIS2_PLACEMENT_3D('',#2086,#1693,#1694);
#1390=AXIS2_PLACEMENT_3D('',#2088,#1696,#1697);
#1391=AXIS2_PLACEMENT_3D('',#2090,#1699,#1700);
#1392=AXIS2_PLACEMENT_3D('',#2091,#1701,#1702);
#1393=AXIS2_PLACEMENT_3D('',#2093,#1704,#1705);
#1465=DIRECTION('axis',(0.,0.,1.));
#1466=DIRECTION('refdir',(1.,0.,0.));
#1467=DIRECTION('center_axis',(0.,-1.,0.));
#1468=DIRECTION('ref_axis',(1.,0.,0.));
#1469=DIRECTION('center_axis',(0.,-1.,0.));
#1470=DIRECTION('ref_axis',(1.,0.,0.));
#1471=DIRECTION('',(0.,-1.,0.));
#1472=DIRECTION('center_axis',(0.,1.,0.));
#1473=DIRECTION('ref_axis',(1.,0.,0.));
#1474=DIRECTION('center_axis',(0.,-1.,0.));
#1475=DIRECTION('ref_axis',(0.499999999999999,0.,-0.866025403784439));
#1476=DIRECTION('',(0.,1.,0.));
#1477=DIRECTION('center_axis',(0.,1.,0.));
#1478=DIRECTION('ref_axis',(0.499999999999999,0.,-0.866025403784439));
#1479=DIRECTION('',(0.,-1.,0.));
#1480=DIRECTION('center_axis',(0.,-1.,0.));
#1481=DIRECTION('ref_axis',(0.499999999999999,0.,-0.866025403784439));
#1482=DIRECTION('center_axis',(0.,-1.,0.));
#1483=DIRECTION('ref_axis',(-0.5,0.,-0.866025403784438));
#1484=DIRECTION('',(0.,1.,0.));
#1485=DIRECTION('center_axis',(0.,1.,0.));
#1486=DIRECTION('ref_axis',(-0.5,0.,-0.866025403784438));
#1487=DIRECTION('',(0.,-1.,0.));
#1488=DIRECTION('center_axis',(0.,-1.,0.));
#1489=DIRECTION('ref_axis',(-0.5,0.,-0.866025403784438));
#1490=DIRECTION('center_axis',(0.,-1.,0.));
#1491=DIRECTION('ref_axis',(-1.,0.,8.54017711250121E-17));
#1492=DIRECTION('',(0.,1.,0.));
#1493=DIRECTION('center_axis',(0.,1.,0.));
#1494=DIRECTION('ref_axis',(-1.,0.,8.54017711250121E-17));
#1495=DIRECTION('',(0.,-1.,0.));
#1496=DIRECTION('center_axis',(0.,-1.,0.));
#1497=DIRECTION('ref_axis',(-1.,0.,8.54017711250121E-17));
#1498=DIRECTION('center_axis',(0.,-1.,0.));
#1499=DIRECTION('ref_axis',(-0.5,0.,0.866025403784439));
#1500=DIRECTION('',(0.,1.,0.));
#1501=DIRECTION('center_axis',(0.,1.,0.));
#1502=DIRECTION('ref_axis',(-0.5,0.,0.866025403784439));
#1503=DIRECTION('',(0.,-1.,0.));
#1504=DIRECTION('center_axis',(0.,-1.,0.));
#1505=DIRECTION('ref_axis',(-0.5,0.,0.866025403784439));
#1506=DIRECTION('center_axis',(0.,-1.,0.));
#1507=DIRECTION('ref_axis',(0.5,0.,0.866025403784439));
#1508=DIRECTION('',(0.,1.,0.));
#1509=DIRECTION('center_axis',(0.,1.,0.));
#1510=DIRECTION('ref_axis',(0.5,0.,0.866025403784439));
#1511=DIRECTION('',(0.,-1.,0.));
#1512=DIRECTION('center_axis',(0.,-1.,0.));
#1513=DIRECTION('ref_axis',(0.5,0.,0.866025403784439));
#1514=DIRECTION('center_axis',(0.,-1.,0.));
#1515=DIRECTION('ref_axis',(-1.,0.,0.));
#1516=DIRECTION('center_axis',(0.,-1.,0.));
#1517=DIRECTION('ref_axis',(-1.,0.,0.));
#1518=DIRECTION('',(0.,-1.,0.));
#1519=DIRECTION('center_axis',(0.,1.,0.));
#1520=DIRECTION('ref_axis',(-1.,0.,0.));
#1521=DIRECTION('center_axis',(0.,1.,0.));
#1522=DIRECTION('ref_axis',(-1.,0.,0.));
#1523=DIRECTION('center_axis',(0.,1.,0.));
#1524=DIRECTION('ref_axis',(-1.,0.,0.));
#1525=DIRECTION('',(0.,-1.,0.));
#1526=DIRECTION('center_axis',(0.,-1.,0.));
#1527=DIRECTION('ref_axis',(-1.,0.,0.));
#1528=DIRECTION('center_axis',(0.,-1.,0.));
#1529=DIRECTION('ref_axis',(1.,0.,0.));
#1530=DIRECTION('center_axis',(0.,-1.,0.));
#1531=DIRECTION('ref_axis',(1.,0.,0.));
#1532=DIRECTION('',(0.,-1.,0.));
#1533=DIRECTION('center_axis',(0.,1.,0.));
#1534=DIRECTION('ref_axis',(1.,0.,0.));
#1535=DIRECTION('center_axis',(0.,-1.,0.));
#1536=DIRECTION('ref_axis',(1.,0.,0.));
#1537=DIRECTION('center_axis',(0.,-1.,0.));
#1538=DIRECTION('ref_axis',(1.,0.,0.));
#1539=DIRECTION('',(0.,-1.,0.));
#1540=DIRECTION('center_axis',(0.,1.,0.));
#1541=DIRECTION('ref_axis',(1.,0.,0.));
#1542=DIRECTION('center_axis',(0.,1.,0.));
#1543=DIRECTION('ref_axis',(1.,0.,0.));
#1544=DIRECTION('',(-1.,0.,0.));
#1545=DIRECTION('center_axis',(0.,-1.,0.));
#1546=DIRECTION('ref_axis',(-8.88178419700125E-16,0.,-1.));
#1547=DIRECTION('',(-1.,0.,0.));
#1548=DIRECTION('center_axis',(0.,-1.,0.));
#1549=DIRECTION('ref_axis',(-1.,0.,0.));
#1550=DIRECTION('',(0.5,0.,-0.866025403784439));
#1551=DIRECTION('center_axis',(0.,-1.,0.));
#1552=DIRECTION('ref_axis',(-0.866025403784439,0.,-0.5));
#1553=DIRECTION('',(-0.5,0.,0.866025403784439));
#1554=DIRECTION('center_axis',(0.,1.,0.));
#1555=DIRECTION('ref_axis',(1.,0.,0.));
#1556=DIRECTION('',(0.5,0.,0.866025403784439));
#1557=DIRECTION('center_axis',(0.,1.,0.));
#1558=DIRECTION('ref_axis',(0.866025403784439,0.,-0.5));
#1559=DIRECTION('',(-0.5,0.,-0.866025403784439));
#1560=DIRECTION('center_axis',(0.,1.,0.));
#1561=DIRECTION('ref_axis',(1.,0.,0.));
#1562=DIRECTION('',(1.,0.,0.));
#1563=DIRECTION('center_axis',(0.,1.,0.));
#1564=DIRECTION('ref_axis',(8.88178419700125E-16,0.,-1.));
#1565=DIRECTION('',(1.,0.,0.));
#1566=DIRECTION('center_axis',(0.,-1.,0.));
#1567=DIRECTION('ref_axis',(1.,0.,0.));
#1568=DIRECTION('center_axis',(0.,-1.,0.));
#1569=DIRECTION('ref_axis',(1.,0.,0.));
#1570=DIRECTION('',(-0.5,0.,0.866025403784439));
#1571=DIRECTION('center_axis',(0.,-1.,0.));
#1572=DIRECTION('ref_axis',(0.866025403784439,0.,0.5));
#1573=DIRECTION('',(0.5,0.,-0.866025403784439));
#1574=DIRECTION('center_axis',(0.,-1.,0.));
#1575=DIRECTION('ref_axis',(1.,0.,0.));
#1576=DIRECTION('center_axis',(0.,-1.,0.));
#1577=DIRECTION('ref_axis',(1.,0.,0.));
#1578=DIRECTION('center_axis',(0.,-1.,0.));
#1579=DIRECTION('ref_axis',(1.,0.,0.));
#1580=DIRECTION('',(-0.5,0.,-0.866025403784439));
#1581=DIRECTION('center_axis',(0.,1.,0.));
#1582=DIRECTION('ref_axis',(-0.866025403784439,0.,0.5));
#1583=DIRECTION('',(0.5,0.,0.866025403784439));
#1584=DIRECTION('center_axis',(0.,1.,0.));
#1585=DIRECTION('ref_axis',(-1.,0.,0.));
#1586=DIRECTION('center_axis',(0.,1.,0.));
#1587=DIRECTION('ref_axis',(1.,0.,0.));
#1588=DIRECTION('center_axis',(0.,1.,0.));
#1589=DIRECTION('ref_axis',(1.,0.,0.));
#1590=DIRECTION('',(0.,-1.,0.));
#1591=DIRECTION('center_axis',(0.,-1.,0.));
#1592=DIRECTION('ref_axis',(1.,0.,0.));
#1593=DIRECTION('',(0.,-1.,0.));
#1594=DIRECTION('',(0.,1.,0.));
#1595=DIRECTION('center_axis',(0.,1.,0.));
#1596=DIRECTION('ref_axis',(1.,0.,0.));
#1597=DIRECTION('center_axis',(0.,1.,0.));
#1598=DIRECTION('ref_axis',(1.,0.,0.));
#1599=DIRECTION('center_axis',(0.,-1.,0.));
#1600=DIRECTION('ref_axis',(-1.,0.,0.));
#1601=DIRECTION('',(0.5,0.,0.866025403784439));
#1602=DIRECTION('center_axis',(0.,1.,0.));
#1603=DIRECTION('ref_axis',(-0.866025403784439,0.,0.5));
#1604=DIRECTION('',(-0.5,0.,-0.866025403784439));
#1605=DIRECTION('center_axis',(0.,1.,0.));
#1606=DIRECTION('ref_axis',(1.,0.,0.));
#1607=DIRECTION('center_axis',(0.,1.,0.));
#1608=DIRECTION('ref_axis',(1.,0.,0.));
#1609=DIRECTION('',(0.5,0.,-0.866025403784439));
#1610=DIRECTION('center_axis',(0.,-1.,0.));
#1611=DIRECTION('ref_axis',(0.866025403784439,0.,0.5));
#1612=DIRECTION('',(-0.5,0.,0.866025403784439));
#1613=DIRECTION('center_axis',(0.,1.,0.));
#1614=DIRECTION('ref_axis',(1.,0.,0.));
#1615=DIRECTION('',(1.,0.,0.));
#1616=DIRECTION('center_axis',(0.,-1.,0.));
#1617=DIRECTION('ref_axis',(8.88178419700125E-16,0.,1.));
#1618=DIRECTION('',(1.,0.,0.));
#1619=DIRECTION('center_axis',(0.,-1.,0.));
#1620=DIRECTION('ref_axis',(1.,0.,0.));
#1621=DIRECTION('',(-0.5,0.,-0.866025403784439));
#1622=DIRECTION('center_axis',(0.,1.,0.));
#1623=DIRECTION('ref_axis',(0.866025403784439,0.,-0.5));
#1624=DIRECTION('',(0.5,0.,0.866025403784439));
#1625=DIRECTION('center_axis',(0.,-1.,0.));
#1626=DIRECTION('ref_axis',(1.,0.,0.));
#1627=DIRECTION('',(-0.5,0.,0.866025403784439));
#1628=DIRECTION('center_axis',(0.,-1.,0.));
#1629=DIRECTION('ref_axis',(-0.866025403784439,0.,-0.5));
#1630=DIRECTION('',(0.5,0.,-0.866025403784439));
#1631=DIRECTION('center_axis',(0.,1.,0.));
#1632=DIRECTION('ref_axis',(-1.,0.,0.));
#1633=DIRECTION('',(-1.,0.,0.));
#1634=DIRECTION('center_axis',(0.,1.,0.));
#1635=DIRECTION('ref_axis',(-8.88178419700125E-16,0.,1.));
#1636=DIRECTION('',(-1.,0.,0.));
#1637=DIRECTION('center_axis',(0.,1.,0.));
#1638=DIRECTION('ref_axis',(1.,0.,0.));
#1639=DIRECTION('',(0.,-1.,0.));
#1640=DIRECTION('center_axis',(0.,1.,0.));
#1641=DIRECTION('ref_axis',(1.,0.,0.));
#1642=DIRECTION('',(0.,-1.,0.));
#1643=DIRECTION('center_axis',(-0.866025403784439,0.,0.5));
#1644=DIRECTION('ref_axis',(-0.5,0.,-0.866025403784439));
#1645=DIRECTION('',(0.,-1.,0.));
#1646=DIRECTION('center_axis',(0.,-1.,0.));
#1647=DIRECTION('ref_axis',(-0.866025403784439,0.,0.5));
#1648=DIRECTION('',(0.,-1.,0.));
#1649=DIRECTION('center_axis',(0.866025403784439,0.,-0.5));
#1650=DIRECTION('ref_axis',(0.5,0.,0.866025403784439));
#1651=DIRECTION('',(0.,-1.,0.));
#1652=DIRECTION('center_axis',(0.,-1.,0.));
#1653=DIRECTION('ref_axis',(-1.,0.,0.));
#1654=DIRECTION('center_axis',(0.,0.,1.));
#1655=DIRECTION('ref_axis',(-1.,0.,0.));
#1656=DIRECTION('',(0.,-1.,0.));
#1657=DIRECTION('center_axis',(-0.866025403784439,0.,-0.5));
#1658=DIRECTION('ref_axis',(0.5,0.,-0.866025403784439));
#1659=DIRECTION('',(0.,-1.,0.));
#1660=DIRECTION('center_axis',(0.,1.,0.));
#1661=DIRECTION('ref_axis',(0.866025403784439,0.,0.5));
#1662=DIRECTION('',(0.,-1.,0.));
#1663=DIRECTION('center_axis',(0.866025403784439,0.,0.5));
#1664=DIRECTION('ref_axis',(-0.5,0.,0.866025403784439));
#1665=DIRECTION('center_axis',(0.,1.,0.));
#1666=DIRECTION('ref_axis',(1.,0.,0.));
#1667=DIRECTION('',(0.,-1.,0.));
#1668=DIRECTION('center_axis',(0.,0.,-1.));
#1669=DIRECTION('ref_axis',(1.,0.,0.));
#1670=DIRECTION('',(0.,-1.,0.));
#1671=DIRECTION('center_axis',(0.866025403784439,0.,0.5));
#1672=DIRECTION('ref_axis',(-0.5,0.,0.866025403784439));
#1673=DIRECTION('',(0.,-1.,0.));
#1674=DIRECTION('',(0.,-1.,0.));
#1675=DIRECTION('center_axis',(0.,1.,0.));
#1676=DIRECTION('ref_axis',(-0.866025403784439,0.,-0.5));
#1677=DIRECTION('',(0.,-1.,0.));
#1678=DIRECTION('center_axis',(-0.866025403784439,0.,-0.5));
#1679=DIRECTION('ref_axis',(0.5,0.,-0.866025403784439));
#1680=DIRECTION('center_axis',(0.,1.,0.));
#1681=DIRECTION('ref_axis',(-1.,0.,0.));
#1682=DIRECTION('',(0.,-1.,0.));
#1683=DIRECTION('center_axis',(0.,0.,1.));
#1684=DIRECTION('ref_axis',(-1.,0.,0.));
#1685=DIRECTION('',(0.,-1.,0.));
#1686=DIRECTION('center_axis',(0.,1.,0.));
#1687=DIRECTION('ref_axis',(-8.88178419700125E-16,0.,-1.));
#1688=DIRECTION('center_axis',(0.,-1.,0.));
#1689=DIRECTION('ref_axis',(1.,0.,0.));
#1690=DIRECTION('center_axis',(0.866025403784439,0.,-0.5));
#1691=DIRECTION('ref_axis',(0.5,0.,0.866025403784439));
#1692=DIRECTION('',(0.,-1.,0.));
#1693=DIRECTION('center_axis',(0.,-1.,0.));
#1694=DIRECTION('ref_axis',(0.866025403784439,0.,-0.5));
#1695=DIRECTION('',(0.,-1.,0.));
#1696=DIRECTION('center_axis',(-0.866025403784439,0.,0.5));
#1697=DIRECTION('ref_axis',(-0.5,0.,-0.866025403784439));
#1698=DIRECTION('',(0.,-1.,0.));
#1699=DIRECTION('center_axis',(0.,-1.,0.));
#1700=DIRECTION('ref_axis',(1.,0.,0.));
#1701=DIRECTION('center_axis',(0.,0.,-1.));
#1702=DIRECTION('ref_axis',(1.,0.,0.));
#1703=DIRECTION('',(0.,-1.,0.));
#1704=DIRECTION('center_axis',(0.,-1.,0.));
#1705=DIRECTION('ref_axis',(8.88178419700125E-16,0.,-1.));
#1869=CARTESIAN_POINT('',(0.,0.,0.));
#1870=CARTESIAN_POINT('Origin',(0.,0.,64.2867316297599));
#1871=CARTESIAN_POINT('',(-2.5,0.,64.2867316297599));
#1872=CARTESIAN_POINT('Origin',(0.,0.,64.2867316297599));
#1873=CARTESIAN_POINT('',(-2.5,-5.,64.2867316297599));
#1874=CARTESIAN_POINT('',(-2.5,0.,64.2867316297599));
#1875=CARTESIAN_POINT('Origin',(0.,-5.,64.2867316297599));
#1876=CARTESIAN_POINT('Origin',(-34.7405684710615,0.,44.2292550711919));
#1877=CARTESIAN_POINT('',(-23.2587346574158,-5.,38.1327403065235));
#1878=CARTESIAN_POINT('',(-23.2587346574158,0.,38.1327403065235));
#1879=CARTESIAN_POINT('',(-23.2587346574158,0.,38.1327403065235));
#1880=CARTESIAN_POINT('',(-34.2793882249884,-5.,57.2210722181746));
#1881=CARTESIAN_POINT('Origin',(-34.7405684710615,-5.,44.2292550711919));
#1882=CARTESIAN_POINT('',(-34.2793882249884,0.,57.2210722181746));
#1883=CARTESIAN_POINT('',(-34.2793882249884,0.,57.2210722181746));
#1884=CARTESIAN_POINT('Origin',(-34.7405684710615,0.,44.2292550711919));
#1885=CARTESIAN_POINT('Origin',(-34.7405684710615,0.,84.3442081883279));
#1886=CARTESIAN_POINT('',(-34.2793882249884,-5.,71.3523910413453));
#1887=CARTESIAN_POINT('',(-34.2793882249884,0.,71.3523910413453));
#1888=CARTESIAN_POINT('',(-34.2793882249884,0.,71.3523910413453));
#1889=CARTESIAN_POINT('',(-23.2587346574157,-5.,90.4407229529964));
#1890=CARTESIAN_POINT('Origin',(-34.7405684710615,-5.,84.3442081883279));
#1891=CARTESIAN_POINT('',(-23.2587346574157,0.,90.4407229529964));
#1892=CARTESIAN_POINT('',(-23.2587346574157,0.,90.4407229529964));
#1893=CARTESIAN_POINT('Origin',(-34.7405684710615,0.,84.3442081883279));
#1894=CARTESIAN_POINT('Origin',(-8.88178419700125E-15,0.,104.401684746896));
#1895=CARTESIAN_POINT('',(-11.0206535675727,-5.,97.5063823645817));
#1896=CARTESIAN_POINT('',(-11.0206535675727,0.,97.5063823645817));
#1897=CARTESIAN_POINT('',(-11.0206535675727,0.,97.5063823645817));
#1898=CARTESIAN_POINT('',(11.0206535675727,-5.,97.5063823645817));
#1899=CARTESIAN_POINT('Origin',(-8.88178419700125E-15,-5.,104.401684746896));
#1900=CARTESIAN_POINT('',(11.0206535675727,0.,97.5063823645817));
#1901=CARTESIAN_POINT('',(11.0206535675727,0.,97.5063823645817));
#1902=CARTESIAN_POINT('Origin',(-8.88178419700125E-15,0.,104.401684746896));
#1903=CARTESIAN_POINT('Origin',(34.7405684710615,0.,84.3442081883279));
#1904=CARTESIAN_POINT('',(23.2587346574158,-5.,90.4407229529964));
#1905=CARTESIAN_POINT('',(23.2587346574158,0.,90.4407229529964));
#1906=CARTESIAN_POINT('',(23.2587346574158,0.,90.4407229529964));
#1907=CARTESIAN_POINT('',(34.2793882249884,-5.,71.3523910413453));
#1908=CARTESIAN_POINT('Origin',(34.7405684710615,-5.,84.3442081883279));
#1909=CARTESIAN_POINT('',(34.2793882249884,0.,71.3523910413453));
#1910=CARTESIAN_POINT('',(34.2793882249884,0.,71.3523910413453));
#1911=CARTESIAN_POINT('Origin',(34.7405684710615,0.,84.3442081883279));
#1912=CARTESIAN_POINT('Origin',(34.7405684710615,0.,44.2292550711919));
#1913=CARTESIAN_POINT('',(34.2793882249884,-5.,57.2210722181745));
#1914=CARTESIAN_POINT('',(34.2793882249884,0.,57.2210722181745));
#1915=CARTESIAN_POINT('',(34.2793882249884,0.,57.2210722181745));
#1916=CARTESIAN_POINT('',(23.2587346574157,-5.,38.1327403065234));
#1917=CARTESIAN_POINT('Origin',(34.7405684710615,-5.,44.2292550711919));
#1918=CARTESIAN_POINT('',(23.2587346574157,0.,38.1327403065234));
#1919=CARTESIAN_POINT('',(23.2587346574157,0.,38.1327403065234));
#1920=CARTESIAN_POINT('Origin',(34.7405684710615,0.,44.2292550711919));
#1921=CARTESIAN_POINT('Origin',(0.,0.,64.2867316297599));
#1922=CARTESIAN_POINT('',(-34.9106001094224,-5.,61.7867316297599));
#1923=CARTESIAN_POINT('Origin',(0.,-5.,64.2867316297599));
#1924=CARTESIAN_POINT('',(-34.9106001094224,0.,61.7867316297599));
#1925=CARTESIAN_POINT('',(-34.9106001094224,0.,61.7867316297599));
#1926=CARTESIAN_POINT('Origin',(0.,0.,64.2867316297599));
#1927=CARTESIAN_POINT('Origin',(0.,0.,64.2867316297599));
#1928=CARTESIAN_POINT('',(-19.6203635641723,-5.,93.2701981858795));
#1929=CARTESIAN_POINT('Origin',(0.,-5.,64.2867316297599));
#1930=CARTESIAN_POINT('',(-19.6203635641723,0.,93.2701981858795));
#1931=CARTESIAN_POINT('',(-19.6203635641723,0.,93.2701981858795));
#1932=CARTESIAN_POINT('Origin',(0.,0.,64.2867316297599));
#1933=CARTESIAN_POINT('Origin',(0.,0.,64.2867316297599));
#1934=CARTESIAN_POINT('',(15.2902365452501,-5.,95.7701981858795));
#1935=CARTESIAN_POINT('Origin',(0.,-5.,64.2867316297599));
#1936=CARTESIAN_POINT('',(15.2902365452501,0.,95.7701981858795));
#1937=CARTESIAN_POINT('',(15.2902365452501,0.,95.7701981858795));
#1938=CARTESIAN_POINT('Origin',(0.,0.,64.2867316297599));
#1939=CARTESIAN_POINT('Origin',(0.,0.,64.2867316297599));
#1940=CARTESIAN_POINT('',(34.9106001094224,-5.,66.7867316297599));
#1941=CARTESIAN_POINT('Origin',(0.,-5.,64.2867316297599));
#1942=CARTESIAN_POINT('',(34.9106001094224,0.,66.7867316297599));
#1943=CARTESIAN_POINT('',(34.9106001094224,0.,66.7867316297599));
#1944=CARTESIAN_POINT('Origin',(0.,0.,64.2867316297599));
#1945=CARTESIAN_POINT('Origin',(17.4553000547112,0.,81.7867316297599));
#1946=CARTESIAN_POINT('',(-13.316088815901,0.,61.7867316297599));
#1947=CARTESIAN_POINT('',(-13.316088815901,0.,61.7867316297599));
#1948=CARTESIAN_POINT('',(-13.316088815901,0.,66.7867316297599));
#1949=CARTESIAN_POINT('Origin',(-13.316088815901,0.,64.2867316297599));
#1950=CARTESIAN_POINT('',(-34.9106001094224,0.,66.7867316297599));
#1951=CARTESIAN_POINT('',(-13.316088815901,0.,66.7867316297599));
#1952=CARTESIAN_POINT('Origin',(0.,0.,64.2867316297599));
#1953=CARTESIAN_POINT('',(-8.82310791741161,0.,74.56880282338));
#1954=CARTESIAN_POINT('',(-22.4951260134151,0.,98.2494328076592));
#1955=CARTESIAN_POINT('',(-4.49298089848941,0.,77.06880282338));
#1956=CARTESIAN_POINT('Origin',(-6.65804440795051,0.,75.81880282338));
#1957=CARTESIAN_POINT('',(-15.2902365452501,0.,95.7701981858795));
#1958=CARTESIAN_POINT('',(-4.49298089848941,0.,77.06880282338));
#1959=CARTESIAN_POINT('Origin',(0.,0.,64.2867316297599));
#1960=CARTESIAN_POINT('',(4.49298089848941,0.,77.06880282338));
#1961=CARTESIAN_POINT('',(4.49298089848941,0.,77.06880282338));
#1962=CARTESIAN_POINT('',(8.82310791741161,0.,74.56880282338));
#1963=CARTESIAN_POINT('Origin',(6.65804440795051,0.,75.81880282338));
#1964=CARTESIAN_POINT('',(19.6203635641723,0.,93.2701981858795));
#1965=CARTESIAN_POINT('',(22.4951260134151,0.,98.2494328076592));
#1966=CARTESIAN_POINT('Origin',(0.,0.,64.2867316297599));
#1967=CARTESIAN_POINT('',(13.316088815901,0.,66.7867316297599));
#1968=CARTESIAN_POINT('',(13.316088815901,0.,66.7867316297599));
#1969=CARTESIAN_POINT('',(13.316088815901,0.,61.7867316297599));
#1970=CARTESIAN_POINT('Origin',(13.316088815901,0.,64.2867316297599));
#1971=CARTESIAN_POINT('',(34.9106001094224,0.,61.7867316297599));
#1972=CARTESIAN_POINT('',(13.316088815901,0.,61.7867316297599));
#1973=CARTESIAN_POINT('Origin',(0.,0.,64.2867316297599));
#1974=CARTESIAN_POINT('',(19.6203635641723,0.,35.3032650736403));
#1975=CARTESIAN_POINT('Origin',(0.,0.,64.2867316297599));
#1976=CARTESIAN_POINT('',(8.82310791741161,0.,54.0046604361398));
#1977=CARTESIAN_POINT('',(22.4951260134151,0.,30.3240304518606));
#1978=CARTESIAN_POINT('',(4.49298089848941,0.,51.5046604361398));
#1979=CARTESIAN_POINT('Origin',(6.65804440795051,0.,52.7546604361398));
#1980=CARTESIAN_POINT('',(15.2902365452501,0.,32.8032650736403));
#1981=CARTESIAN_POINT('',(4.49298089848941,0.,51.5046604361398));
#1982=CARTESIAN_POINT('',(11.0206535675727,0.,31.0670808949381));
#1983=CARTESIAN_POINT('Origin',(0.,0.,64.2867316297599));
#1984=CARTESIAN_POINT('',(-11.0206535675727,0.,31.0670808949381));
#1985=CARTESIAN_POINT('Origin',(0.,0.,24.1717785126239));
#1986=CARTESIAN_POINT('',(-15.2902365452501,0.,32.8032650736403));
#1987=CARTESIAN_POINT('Origin',(0.,0.,64.2867316297599));
#1988=CARTESIAN_POINT('',(-4.49298089848941,0.,51.5046604361398));
#1989=CARTESIAN_POINT('',(-4.49298089848941,0.,51.5046604361398));
#1990=CARTESIAN_POINT('',(-8.82310791741161,0.,54.0046604361398));
#1991=CARTESIAN_POINT('Origin',(-6.65804440795051,0.,52.7546604361398));
#1992=CARTESIAN_POINT('',(-19.6203635641723,0.,35.3032650736403));
#1993=CARTESIAN_POINT('',(-22.4951260134151,0.,30.3240304518606));
#1994=CARTESIAN_POINT('Origin',(0.,0.,64.2867316297599));
#1995=CARTESIAN_POINT('Origin',(0.,0.,64.2867316297599));
#1996=CARTESIAN_POINT('',(19.6203635641723,-5.,35.3032650736403));
#1997=CARTESIAN_POINT('Origin',(0.,-5.,64.2867316297599));
#1998=CARTESIAN_POINT('',(19.6203635641723,0.,35.3032650736403));
#1999=CARTESIAN_POINT('Origin',(0.,0.,24.1717785126239));
#2000=CARTESIAN_POINT('',(-11.0206535675727,-5.,31.0670808949381));
#2001=CARTESIAN_POINT('',(-11.0206535675727,0.,31.0670808949381));
#2002=CARTESIAN_POINT('',(11.0206535675727,-5.,31.0670808949381));
#2003=CARTESIAN_POINT('',(11.0206535675727,0.,31.0670808949381));
#2004=CARTESIAN_POINT('Origin',(0.,-5.,24.1717785126239));
#2005=CARTESIAN_POINT('Origin',(17.4553000547112,-5.,81.7867316297599));
#2006=CARTESIAN_POINT('',(-19.6203635641723,-5.,35.3032650736403));
#2007=CARTESIAN_POINT('Origin',(0.,-5.,64.2867316297599));
#2008=CARTESIAN_POINT('',(-8.82310791741161,-5.,54.0046604361398));
#2009=CARTESIAN_POINT('',(-22.4951260134151,-5.,30.3240304518606));
#2010=CARTESIAN_POINT('',(-4.49298089848941,-5.,51.5046604361398));
#2011=CARTESIAN_POINT('Origin',(-6.65804440795051,-5.,52.7546604361398));
#2012=CARTESIAN_POINT('',(-15.2902365452501,-5.,32.8032650736403));
#2013=CARTESIAN_POINT('',(-4.49298089848941,-5.,51.5046604361398));
#2014=CARTESIAN_POINT('Origin',(0.,-5.,64.2867316297599));
#2015=CARTESIAN_POINT('',(15.2902365452501,-5.,32.8032650736403));
#2016=CARTESIAN_POINT('Origin',(0.,-5.,64.2867316297599));
#2017=CARTESIAN_POINT('',(4.49298089848941,-5.,51.5046604361398));
#2018=CARTESIAN_POINT('',(4.49298089848941,-5.,51.5046604361398));
#2019=CARTESIAN_POINT('',(8.82310791741161,-5.,54.0046604361398));
#2020=CARTESIAN_POINT('Origin',(6.65804440795051,-5.,52.7546604361398));
#2021=CARTESIAN_POINT('',(22.4951260134151,-5.,30.3240304518606));
#2022=CARTESIAN_POINT('',(34.9106001094224,-5.,61.7867316297599));
#2023=CARTESIAN_POINT('Origin',(0.,-5.,64.2867316297599));
#2024=CARTESIAN_POINT('',(13.316088815901,-5.,61.7867316297599));
#2025=CARTESIAN_POINT('',(13.316088815901,-5.,61.7867316297599));
#2026=CARTESIAN_POINT('',(13.316088815901,-5.,66.7867316297599));
#2027=CARTESIAN_POINT('Origin',(13.316088815901,-5.,64.2867316297599));
#2028=CARTESIAN_POINT('',(13.316088815901,-5.,66.7867316297599));
#2029=CARTESIAN_POINT('',(19.6203635641723,-5.,93.2701981858795));
#2030=CARTESIAN_POINT('Origin',(0.,-5.,64.2867316297599));
#2031=CARTESIAN_POINT('',(8.82310791741161,-5.,74.56880282338));
#2032=CARTESIAN_POINT('',(22.4951260134151,-5.,98.2494328076592));
#2033=CARTESIAN_POINT('',(4.49298089848941,-5.,77.06880282338));
#2034=CARTESIAN_POINT('Origin',(6.65804440795051,-5.,75.81880282338));
#2035=CARTESIAN_POINT('',(4.49298089848941,-5.,77.06880282338));
#2036=CARTESIAN_POINT('',(-15.2902365452501,-5.,95.7701981858795));
#2037=CARTESIAN_POINT('Origin',(0.,-5.,64.2867316297599));
#2038=CARTESIAN_POINT('',(-4.49298089848941,-5.,77.06880282338));
#2039=CARTESIAN_POINT('',(-4.49298089848941,-5.,77.06880282338));
#2040=CARTESIAN_POINT('',(-8.82310791741161,-5.,74.56880282338));
#2041=CARTESIAN_POINT('Origin',(-6.65804440795051,-5.,75.81880282338));
#2042=CARTESIAN_POINT('',(-22.4951260134151,-5.,98.2494328076592));
#2043=CARTESIAN_POINT('',(-34.9106001094224,-5.,66.7867316297599));
#2044=CARTESIAN_POINT('Origin',(0.,-5.,64.2867316297599));
#2045=CARTESIAN_POINT('',(-13.316088815901,-5.,66.7867316297599));
#2046=CARTESIAN_POINT('',(-13.316088815901,-5.,66.7867316297599));
#2047=CARTESIAN_POINT('',(-13.316088815901,-5.,61.7867316297599));
#2048=CARTESIAN_POINT('Origin',(-13.316088815901,-5.,64.2867316297599));
#2049=CARTESIAN_POINT('',(-13.316088815901,-5.,61.7867316297599));
#2050=CARTESIAN_POINT('Origin',(0.,0.,64.2867316297599));
#2051=CARTESIAN_POINT('',(15.2902365452501,0.,32.8032650736403));
#2052=CARTESIAN_POINT('Origin',(0.,0.,64.2867316297599));
#2053=CARTESIAN_POINT('',(-15.2902365452501,0.,32.8032650736403));
#2054=CARTESIAN_POINT('Origin',(-4.49298089848941,0.,51.5046604361398));
#2055=CARTESIAN_POINT('',(-4.49298089848941,0.,51.5046604361398));
#2056=CARTESIAN_POINT('Origin',(-6.65804440795051,0.,52.7546604361398));
#2057=CARTESIAN_POINT('',(-8.82310791741161,0.,54.0046604361398));
#2058=CARTESIAN_POINT('Origin',(-19.6203635641723,0.,35.3032650736403));
#2059=CARTESIAN_POINT('',(-19.6203635641723,0.,35.3032650736403));
#2060=CARTESIAN_POINT('Origin',(0.,0.,64.2867316297599));
#2061=CARTESIAN_POINT('Origin',(-13.316088815901,0.,61.7867316297599));
#2062=CARTESIAN_POINT('',(-13.316088815901,0.,61.7867316297599));
#2063=CARTESIAN_POINT('Origin',(4.49298089848941,0.,51.5046604361398));
#2064=CARTESIAN_POINT('',(4.49298089848941,0.,51.5046604361398));
#2065=CARTESIAN_POINT('Origin',(6.65804440795051,0.,52.7546604361398));
#2066=CARTESIAN_POINT('',(8.82310791741161,0.,54.0046604361398));
#2067=CARTESIAN_POINT('Origin',(19.6203635641723,0.,35.3032650736403));
#2068=CARTESIAN_POINT('Origin',(0.,0.,64.2867316297599));
#2069=CARTESIAN_POINT('',(34.9106001094224,0.,61.7867316297599));
#2070=CARTESIAN_POINT('Origin',(13.316088815901,0.,61.7867316297599));
#2071=CARTESIAN_POINT('',(13.316088815901,0.,61.7867316297599));
#2072=CARTESIAN_POINT('Origin',(-4.49298089848941,0.,77.06880282338));
#2073=CARTESIAN_POINT('',(-4.49298089848941,0.,77.06880282338));
#2074=CARTESIAN_POINT('',(-15.2902365452501,0.,95.7701981858795));
#2075=CARTESIAN_POINT('Origin',(-6.65804440795051,0.,75.81880282338));
#2076=CARTESIAN_POINT('',(-8.82310791741161,0.,74.56880282338));
#2077=CARTESIAN_POINT('Origin',(-19.6203635641723,0.,93.2701981858795));
#2078=CARTESIAN_POINT('Origin',(0.,0.,64.2867316297599));
#2079=CARTESIAN_POINT('',(-34.9106001094224,0.,66.7867316297599));
#2080=CARTESIAN_POINT('Origin',(-13.316088815901,0.,66.7867316297599));
#2081=CARTESIAN_POINT('',(-13.316088815901,0.,66.7867316297599));
#2082=CARTESIAN_POINT('Origin',(-13.316088815901,0.,64.2867316297599));
#2083=CARTESIAN_POINT('Origin',(0.,0.,64.2867316297599));
#2084=CARTESIAN_POINT('Origin',(4.49298089848941,0.,77.06880282338));
#2085=CARTESIAN_POINT('',(4.49298089848941,0.,77.06880282338));
#2086=CARTESIAN_POINT('Origin',(6.65804440795051,0.,75.81880282338));
#2087=CARTESIAN_POINT('',(8.82310791741161,0.,74.56880282338));
#2088=CARTESIAN_POINT('Origin',(19.6203635641723,0.,93.2701981858795));
#2089=CARTESIAN_POINT('',(19.6203635641723,0.,93.2701981858795));
#2090=CARTESIAN_POINT('Origin',(0.,0.,64.2867316297599));
#2091=CARTESIAN_POINT('Origin',(13.316088815901,0.,66.7867316297599));
#2092=CARTESIAN_POINT('',(13.316088815901,0.,66.7867316297599));
#2093=CARTESIAN_POINT('Origin',(13.316088815901,0.,64.2867316297599));
#2220=UNCERTAINTY_MEASURE_WITH_UNIT(LENGTH_MEASURE(0.01),#2239,
'DISTANCE_ACCURACY_VALUE',
'Maximum model space distance between geometric entities at asserted c
onnectivities');
#2228=UNCERTAINTY_MEASURE_WITH_UNIT(LENGTH_MEASURE(0.01),#2239,
'DISTANCE_ACCURACY_VALUE',
'Maximum model space distance between geometric entities at asserted c
onnectivities');
#2230=(
GEOMETRIC_REPRESENTATION_CONTEXT(3)
GLOBAL_UNCERTAINTY_ASSIGNED_CONTEXT((#2220))
GLOBAL_UNIT_ASSIGNED_CONTEXT((#2239,#2241,#2242))
REPRESENTATION_CONTEXT('','3D')
);
#2238=(
GEOMETRIC_REPRESENTATION_CONTEXT(3)
GLOBAL_UNCERTAINTY_ASSIGNED_CONTEXT((#2228))
GLOBAL_UNIT_ASSIGNED_CONTEXT((#2239,#2241,#2242))
REPRESENTATION_CONTEXT('','3D')
);
#2239=(
LENGTH_UNIT()
NAMED_UNIT(*)
SI_UNIT(.MILLI.,.METRE.)
);
#2241=(
NAMED_UNIT(*)
PLANE_ANGLE_UNIT()
SI_UNIT($,.RADIAN.)
);
#2242=(
NAMED_UNIT(*)
SI_UNIT($,.STERADIAN.)
SOLID_ANGLE_UNIT()
);
#2244=SHAPE_DEFINITION_REPRESENTATION(#2253,#2270);
#2253=PRODUCT_DEFINITION_SHAPE('',$,#2280);
#2270=SHAPE_REPRESENTATION('',(#1304),#2230);
#2278=PRODUCT_DEFINITION_CONTEXT('part definition',#2307,'design');
#2280=PRODUCT_DEFINITION('Wheel','Wheel',#2289,#2278);
#2289=PRODUCT_DEFINITION_FORMATION('',$,#2310);
#2307=APPLICATION_CONTEXT(
'Core Data for Automotive Mechanical Design Process');
#2308=PRODUCT_CONTEXT('part definition',#2307,'mechanical');
#2310=PRODUCT('Wheel','Wheel',$,(#2308));
#2319=PRESENTATION_STYLE_ASSIGNMENT((#2323));
#2323=SURFACE_STYLE_USAGE(.BOTH.,#2327);
#2327=SURFACE_SIDE_STYLE('',(#2331));
#2331=SURFACE_STYLE_FILL_AREA(#2335);
#2335=FILL_AREA_STYLE('Surface - Matte',(#2339));
#2339=FILL_AREA_STYLE_COLOUR('Surface - Matte',#2343);
#2343=COLOUR_RGB('Surface - Matte', 0.09019608, 0.27058824, 0.51372549);
ENDSEC;
END-ISO-10303-21;
